ISO-10303-21;
HEADER;
/* Generated by software containing ST-Developer
 * from STEP Tools, Inc. (www.steptools.com) 
 */

FILE_DESCRIPTION(
/* description */ (''),
/* implementation_level */ '2;1');

FILE_NAME(
/* name */ '11_Spindle_Tang_Washer_1in.step',
/* time_stamp */ '2026-10-25T01:26:34-07:00',
/* author */ (''),
/* organization */ (''),
/* preprocessor_version */ 'ST-DEVELOPER v20.2',
/* originating_system */ 'Autodesk Translation Framework v15.15.0.0',
/* authorisation */ '');

FILE_SCHEMA (('AUTOMOTIVE_DESIGN { 1 0 10303 214 3 1 1 }'));
ENDSEC;

DATA;
#10=MECHANICAL_DESIGN_GEOMETRIC_PRESENTATION_REPRESENTATION('',(#328),#71628);
#302=SHAPE_REPRESENTATION_RELATIONSHIP('SRR','None',#71690,#315);
#315=ADVANCED_BREP_SHAPE_REPRESENTATION('',(#341),#71622);
#328=STYLED_ITEM('',(#71825),#341);
#341=MANIFOLD_SOLID_BREP('Body1',#34215);
#1290=FACE_BOUND('',#7060,.T.);
#1291=FACE_BOUND('',#7063,.T.);
#2691=PLANE('',#37020);
#2692=PLANE('',#37021);
#2693=PLANE('',#37022);
#2694=PLANE('',#37023);
#2695=PLANE('',#37024);
#2696=PLANE('',#37025);
#2697=PLANE('',#37030);
#3068=CYLINDRICAL_SURFACE('',#37028,13.6);
#3069=CYLINDRICAL_SURFACE('',#37034,20.5);
#4799=FACE_OUTER_BOUND('',#7054,.T.);
#4800=FACE_OUTER_BOUND('',#7055,.T.);
#4801=FACE_OUTER_BOUND('',#7056,.T.);
#4802=FACE_OUTER_BOUND('',#7057,.T.);
#4803=FACE_OUTER_BOUND('',#7058,.T.);
#4804=FACE_OUTER_BOUND('',#7059,.T.);
#4805=FACE_OUTER_BOUND('',#7061,.T.);
#4806=FACE_OUTER_BOUND('',#7062,.T.);
#4807=FACE_OUTER_BOUND('',#7064,.T.);
#4808=FACE_OUTER_BOUND('',#7065,.T.);
#4809=FACE_OUTER_BOUND('',#7066,.T.);
#7054=EDGE_LOOP('',(#29752,#29753,#29754,#29755));
#7055=EDGE_LOOP('',(#29756,#29757,#29758,#29759,#29760,#29761));
#7056=EDGE_LOOP('',(#29762,#29763,#29764,#29765));
#7057=EDGE_LOOP('',(#29766,#29767,#29768,#29769));
#7058=EDGE_LOOP('',(#29770,#29771,#29772,#29773,#29774,#29775));
#7059=EDGE_LOOP('',(#29776));
#7060=EDGE_LOOP('',(#29777,#29778,#29779,#29780));
#7061=EDGE_LOOP('',(#29781,#29782,#29783,#29784));
#7062=EDGE_LOOP('',(#29785));
#7063=EDGE_LOOP('',(#29786,#29787,#29788,#29789));
#7064=EDGE_LOOP('',(#29790,#29791,#29792,#29793));
#7065=EDGE_LOOP('',(#29794,#29795,#29796,#29797));
#7066=EDGE_LOOP('',(#29798,#29799,#29800,#29801));
#9963=LINE('',#61929,#13013);
#9964=LINE('',#61931,#13014);
#9965=LINE('',#61933,#13015);
#9966=LINE('',#61934,#13016);
#9967=LINE('',#61937,#13017);
#9968=LINE('',#61939,#13018);
#9969=LINE('',#61941,#13019);
#9970=LINE('',#61943,#13020);
#9971=LINE('',#61944,#13021);
#9972=LINE('',#61947,#13022);
#9973=LINE('',#61948,#13023);
#9974=LINE('',#61951,#13024);
#9975=LINE('',#61952,#13025);
#9976=LINE('',#61955,#13026);
#9977=LINE('',#61957,#13027);
#9978=LINE('',#61958,#13028);
#9979=LINE('',#61971,#13029);
#9980=LINE('',#61975,#13030);
#9981=LINE('',#61977,#13031);
#13013=VECTOR('',#45402,10.);
#13014=VECTOR('',#45403,10.);
#13015=VECTOR('',#45404,10.);
#13016=VECTOR('',#45405,10.);
#13017=VECTOR('',#45408,10.);
#13018=VECTOR('',#45409,10.);
#13019=VECTOR('',#45410,10.);
#13020=VECTOR('',#45411,10.);
#13021=VECTOR('',#45412,10.);
#13022=VECTOR('',#45415,10.);
#13023=VECTOR('',#45416,10.);
#13024=VECTOR('',#45419,10.);
#13025=VECTOR('',#45420,10.);
#13026=VECTOR('',#45423,10.);
#13027=VECTOR('',#45424,10.);
#13028=VECTOR('',#45425,10.);
#13029=VECTOR('',#45444,20.35);
#13030=VECTOR('',#45449,20.5);
#13031=VECTOR('',#45452,20.35);
#14344=CIRCLE('',#37026,20.2);
#14345=CIRCLE('',#37027,13.6);
#14346=CIRCLE('',#37029,13.6);
#14347=CIRCLE('',#37031,20.2);
#14348=CIRCLE('',#37033,20.5);
#14349=CIRCLE('',#37035,20.5);
#16751=VERTEX_POINT('',#61927);
#16752=VERTEX_POINT('',#61928);
#16753=VERTEX_POINT('',#61930);
#16754=VERTEX_POINT('',#61932);
#16755=VERTEX_POINT('',#61936);
#16756=VERTEX_POINT('',#61938);
#16757=VERTEX_POINT('',#61940);
#16758=VERTEX_POINT('',#61942);
#16759=VERTEX_POINT('',#61946);
#16760=VERTEX_POINT('',#61950);
#16761=VERTEX_POINT('',#61954);
#16762=VERTEX_POINT('',#61956);
#16763=VERTEX_POINT('',#61960);
#16764=VERTEX_POINT('',#61966);
#16765=VERTEX_POINT('',#61969);
#16766=VERTEX_POINT('',#61973);
#21190=EDGE_CURVE('',#16751,#16752,#9963,.T.);
#21191=EDGE_CURVE('',#16752,#16753,#9964,.T.);
#21192=EDGE_CURVE('',#16753,#16754,#9965,.T.);
#21193=EDGE_CURVE('',#16754,#16751,#9966,.T.);
#21194=EDGE_CURVE('',#16755,#16751,#9967,.T.);
#21195=EDGE_CURVE('',#16756,#16755,#9968,.T.);
#21196=EDGE_CURVE('',#16756,#16757,#9969,.T.);
#21197=EDGE_CURVE('',#16758,#16757,#9970,.T.);
#21198=EDGE_CURVE('',#16752,#16758,#9971,.T.);
#21199=EDGE_CURVE('',#16759,#16754,#9972,.T.);
#21200=EDGE_CURVE('',#16755,#16759,#9973,.T.);
#21201=EDGE_CURVE('',#16759,#16760,#9974,.T.);
#21202=EDGE_CURVE('',#16760,#16756,#9975,.T.);
#21203=EDGE_CURVE('',#16761,#16753,#9976,.T.);
#21204=EDGE_CURVE('',#16762,#16761,#9977,.T.);
#21205=EDGE_CURVE('',#16762,#16760,#9978,.T.);
#21206=EDGE_CURVE('',#16763,#16763,#14344,.T.);
#21207=EDGE_CURVE('',#16761,#16758,#14345,.T.);
#21208=EDGE_CURVE('',#16762,#16757,#14346,.T.);
#21209=EDGE_CURVE('',#16764,#16764,#14347,.T.);
#21210=EDGE_CURVE('',#16765,#16765,#14348,.T.);
#21211=EDGE_CURVE('',#16765,#16764,#9979,.T.);
#21212=EDGE_CURVE('',#16766,#16766,#14349,.T.);
#21213=EDGE_CURVE('',#16766,#16765,#9980,.T.);
#21214=EDGE_CURVE('',#16763,#16766,#9981,.T.);
#29752=ORIENTED_EDGE('',*,*,#21190,.T.);
#29753=ORIENTED_EDGE('',*,*,#21191,.T.);
#29754=ORIENTED_EDGE('',*,*,#21192,.T.);
#29755=ORIENTED_EDGE('',*,*,#21193,.T.);
#29756=ORIENTED_EDGE('',*,*,#21190,.F.);
#29757=ORIENTED_EDGE('',*,*,#21194,.F.);
#29758=ORIENTED_EDGE('',*,*,#21195,.F.);
#29759=ORIENTED_EDGE('',*,*,#21196,.T.);
#29760=ORIENTED_EDGE('',*,*,#21197,.F.);
#29761=ORIENTED_EDGE('',*,*,#21198,.F.);
#29762=ORIENTED_EDGE('',*,*,#21193,.F.);
#29763=ORIENTED_EDGE('',*,*,#21199,.F.);
#29764=ORIENTED_EDGE('',*,*,#21200,.F.);
#29765=ORIENTED_EDGE('',*,*,#21194,.T.);
#29766=ORIENTED_EDGE('',*,*,#21195,.T.);
#29767=ORIENTED_EDGE('',*,*,#21200,.T.);
#29768=ORIENTED_EDGE('',*,*,#21201,.T.);
#29769=ORIENTED_EDGE('',*,*,#21202,.T.);
#29770=ORIENTED_EDGE('',*,*,#21192,.F.);
#29771=ORIENTED_EDGE('',*,*,#21203,.F.);
#29772=ORIENTED_EDGE('',*,*,#21204,.F.);
#29773=ORIENTED_EDGE('',*,*,#21205,.T.);
#29774=ORIENTED_EDGE('',*,*,#21201,.F.);
#29775=ORIENTED_EDGE('',*,*,#21199,.T.);
#29776=ORIENTED_EDGE('',*,*,#21206,.T.);
#29777=ORIENTED_EDGE('',*,*,#21191,.F.);
#29778=ORIENTED_EDGE('',*,*,#21198,.T.);
#29779=ORIENTED_EDGE('',*,*,#21207,.F.);
#29780=ORIENTED_EDGE('',*,*,#21203,.T.);
#29781=ORIENTED_EDGE('',*,*,#21204,.T.);
#29782=ORIENTED_EDGE('',*,*,#21207,.T.);
#29783=ORIENTED_EDGE('',*,*,#21197,.T.);
#29784=ORIENTED_EDGE('',*,*,#21208,.F.);
#29785=ORIENTED_EDGE('',*,*,#21209,.F.);
#29786=ORIENTED_EDGE('',*,*,#21202,.F.);
#29787=ORIENTED_EDGE('',*,*,#21205,.F.);
#29788=ORIENTED_EDGE('',*,*,#21208,.T.);
#29789=ORIENTED_EDGE('',*,*,#21196,.F.);
#29790=ORIENTED_EDGE('',*,*,#21210,.F.);
#29791=ORIENTED_EDGE('',*,*,#21211,.T.);
#29792=ORIENTED_EDGE('',*,*,#21209,.T.);
#29793=ORIENTED_EDGE('',*,*,#21211,.F.);
#29794=ORIENTED_EDGE('',*,*,#21212,.F.);
#29795=ORIENTED_EDGE('',*,*,#21213,.T.);
#29796=ORIENTED_EDGE('',*,*,#21210,.T.);
#29797=ORIENTED_EDGE('',*,*,#21213,.F.);
#29798=ORIENTED_EDGE('',*,*,#21206,.F.);
#29799=ORIENTED_EDGE('',*,*,#21214,.T.);
#29800=ORIENTED_EDGE('',*,*,#21212,.T.);
#29801=ORIENTED_EDGE('',*,*,#21214,.F.);
#32059=CONICAL_SURFACE('',#37032,20.35,0.982793723247326);
#32060=CONICAL_SURFACE('',#37036,20.35,0.982793723247327);
#33773=ADVANCED_FACE('',(#4799),#2691,.T.);
#33774=ADVANCED_FACE('',(#4800),#2692,.T.);
#33775=ADVANCED_FACE('',(#4801),#2693,.T.);
#33776=ADVANCED_FACE('',(#4802),#2694,.T.);
#33777=ADVANCED_FACE('',(#4803),#2695,.T.);
#33778=ADVANCED_FACE('',(#4804,#1290),#2696,.T.);
#33779=ADVANCED_FACE('',(#4805),#3068,.F.);
#33780=ADVANCED_FACE('',(#4806,#1291),#2697,.T.);
#33781=ADVANCED_FACE('',(#4807),#32059,.T.);
#33782=ADVANCED_FACE('',(#4808),#3069,.T.);
#33783=ADVANCED_FACE('',(#4809),#32060,.T.);
#34215=CLOSED_SHELL('',(#33773,#33774,#33775,#33776,#33777,#33778,#33779,
#33780,#33781,#33782,#33783));
#37019=AXIS2_PLACEMENT_3D('',#61925,#45398,#45399);
#37020=AXIS2_PLACEMENT_3D('',#61926,#45400,#45401);
#37021=AXIS2_PLACEMENT_3D('',#61935,#45406,#45407);
#37022=AXIS2_PLACEMENT_3D('',#61945,#45413,#45414);
#37023=AXIS2_PLACEMENT_3D('',#61949,#45417,#45418);
#37024=AXIS2_PLACEMENT_3D('',#61953,#45421,#45422);
#37025=AXIS2_PLACEMENT_3D('',#61959,#45426,#45427);
#37026=AXIS2_PLACEMENT_3D('',#61961,#45428,#45429);
#37027=AXIS2_PLACEMENT_3D('',#61962,#45430,#45431);
#37028=AXIS2_PLACEMENT_3D('',#61963,#45432,#45433);
#37029=AXIS2_PLACEMENT_3D('',#61964,#45434,#45435);
#37030=AXIS2_PLACEMENT_3D('',#61965,#45436,#45437);
#37031=AXIS2_PLACEMENT_3D('',#61967,#45438,#45439);
#37032=AXIS2_PLACEMENT_3D('',#61968,#45440,#45441);
#37033=AXIS2_PLACEMENT_3D('',#61970,#45442,#45443);
#37034=AXIS2_PLACEMENT_3D('',#61972,#45445,#45446);
#37035=AXIS2_PLACEMENT_3D('',#61974,#45447,#45448);
#37036=AXIS2_PLACEMENT_3D('',#61976,#45450,#45451);
#45398=DIRECTION('axis',(0.,0.,1.));
#45399=DIRECTION('refdir',(1.,0.,0.));
#45400=DIRECTION('center_axis',(0.707106781186548,0.,0.707106781186548));
#45401=DIRECTION('ref_axis',(0.707106781186548,0.,-0.707106781186548));
#45402=DIRECTION('',(0.707106781186547,0.,-0.707106781186547));
#45403=DIRECTION('',(0.,1.,0.));
#45404=DIRECTION('',(-0.707106781186547,0.,0.707106781186547));
#45405=DIRECTION('',(0.,-1.,0.));
#45406=DIRECTION('center_axis',(0.,-1.,0.));
#45407=DIRECTION('ref_axis',(0.,0.,-1.));
#45408=DIRECTION('',(1.,0.,0.));
#45409=DIRECTION('',(0.707106781186547,0.,0.707106781186548));
#45410=DIRECTION('',(0.,0.,-1.));
#45411=DIRECTION('',(-1.,0.,0.));
#45412=DIRECTION('',(0.,0.,-1.));
#45413=DIRECTION('center_axis',(0.,0.,1.));
#45414=DIRECTION('ref_axis',(0.,-1.,0.));
#45415=DIRECTION('',(1.,0.,0.));
#45416=DIRECTION('',(0.,1.,0.));
#45417=DIRECTION('center_axis',(-0.707106781186548,0.,0.707106781186547));
#45418=DIRECTION('ref_axis',(0.707106781186547,0.,0.707106781186548));
#45419=DIRECTION('',(-0.707106781186547,0.,-0.707106781186548));
#45420=DIRECTION('',(0.,-1.,0.));
#45421=DIRECTION('center_axis',(0.,1.,0.));
#45422=DIRECTION('ref_axis',(0.,0.,1.));
#45423=DIRECTION('',(0.,0.,1.));
#45424=DIRECTION('',(1.,0.,0.));
#45425=DIRECTION('',(0.,0.,1.));
#45426=DIRECTION('center_axis',(1.,0.,0.));
#45427=DIRECTION('ref_axis',(0.,0.,-1.));
#45428=DIRECTION('center_axis',(1.,0.,0.));
#45429=DIRECTION('ref_axis',(0.,0.,-1.));
#45430=DIRECTION('center_axis',(1.,0.,0.));
#45431=DIRECTION('ref_axis',(0.,0.,-1.));
#45432=DIRECTION('center_axis',(1.,0.,0.));
#45433=DIRECTION('ref_axis',(0.,6.12323399573677E-17,1.));
#45434=DIRECTION('center_axis',(1.,0.,0.));
#45435=DIRECTION('ref_axis',(0.,0.,-1.));
#45436=DIRECTION('center_axis',(-1.,0.,0.));
#45437=DIRECTION('ref_axis',(0.,0.,1.));
#45438=DIRECTION('center_axis',(1.,0.,0.));
#45439=DIRECTION('ref_axis',(0.,0.,-1.));
#45440=DIRECTION('center_axis',(1.,0.,0.));
#45441=DIRECTION('ref_axis',(0.,1.,0.));
#45442=DIRECTION('center_axis',(1.,0.,0.));
#45443=DIRECTION('ref_axis',(0.,0.,-1.));
#45444=DIRECTION('',(-0.554700196225232,0.832050294337842,1.01896772969045E-16));
#45445=DIRECTION('center_axis',(1.,0.,0.));
#45446=DIRECTION('ref_axis',(0.,1.,0.));
#45447=DIRECTION('center_axis',(1.,0.,0.));
#45448=DIRECTION('ref_axis',(0.,0.,-1.));
#45449=DIRECTION('',(-1.,0.,0.));
#45450=DIRECTION('center_axis',(-1.,0.,0.));
#45451=DIRECTION('ref_axis',(0.,1.,0.));
#45452=DIRECTION('',(-0.554700196225231,-0.832050294337843,-1.01896772969045E-16));
#61925=CARTESIAN_POINT('',(0.,0.,0.));
#61926=CARTESIAN_POINT('Origin',(2.3,8.,-13.));
#61927=CARTESIAN_POINT('',(2.2,-2.4,-12.9));
#61928=CARTESIAN_POINT('',(2.4,-2.4,-13.1));
#61929=CARTESIAN_POINT('',(1.7,-2.4,-12.4));
#61930=CARTESIAN_POINT('',(2.4,2.4,-13.1));
#61931=CARTESIAN_POINT('',(2.4,8.,-13.1));
#61932=CARTESIAN_POINT('',(2.2,2.4,-12.9));
#61933=CARTESIAN_POINT('',(1.9,2.4,-12.6));
#61934=CARTESIAN_POINT('',(2.2,8.,-12.9));
#61935=CARTESIAN_POINT('Origin',(0.,-2.4,-12.9));
#61936=CARTESIAN_POINT('',(0.2,-2.4,-12.9));
#61937=CARTESIAN_POINT('',(0.,-2.4,-12.9));
#61938=CARTESIAN_POINT('',(0.,-2.4,-13.1));
#61939=CARTESIAN_POINT('',(0.1,-2.4,-13.));
#61940=CARTESIAN_POINT('',(0.,-2.4,-13.3865604245452));
#61941=CARTESIAN_POINT('',(0.,-2.4,-12.9));
#61942=CARTESIAN_POINT('',(2.4,-2.4,-13.3865604245452));
#61943=CARTESIAN_POINT('',(1.2,-2.4,-13.3865604245452));
#61944=CARTESIAN_POINT('',(2.4,-2.4,-12.9));
#61945=CARTESIAN_POINT('Origin',(0.,2.4,-12.9));
#61946=CARTESIAN_POINT('',(0.2,2.4,-12.9));
#61947=CARTESIAN_POINT('',(0.,2.4,-12.9));
#61948=CARTESIAN_POINT('',(0.2,11.3,-12.9));
#61949=CARTESIAN_POINT('Origin',(0.1,11.3,-13.));
#61950=CARTESIAN_POINT('',(0.,2.4,-13.1));
#61951=CARTESIAN_POINT('',(-0.0999999999999996,2.4,-13.2));
#61952=CARTESIAN_POINT('',(0.,11.3,-13.1));
#61953=CARTESIAN_POINT('Origin',(0.,2.4,-13.7));
#61954=CARTESIAN_POINT('',(2.4,2.4,-13.3865604245452));
#61955=CARTESIAN_POINT('',(2.4,2.4,-13.7));
#61956=CARTESIAN_POINT('',(0.,2.4,-13.3865604245452));
#61957=CARTESIAN_POINT('',(1.2,2.4,-13.3865604245452));
#61958=CARTESIAN_POINT('',(0.,2.4,-13.7));
#61959=CARTESIAN_POINT('Origin',(2.4,13.6,0.));
#61960=CARTESIAN_POINT('',(2.4,-20.2,-2.47378653427765E-15));
#61961=CARTESIAN_POINT('Origin',(2.4,0.,0.));
#61962=CARTESIAN_POINT('Origin',(2.4,0.,0.));
#61963=CARTESIAN_POINT('Origin',(1.2,0.,0.));
#61964=CARTESIAN_POINT('Origin',(0.,0.,0.));
#61965=CARTESIAN_POINT('Origin',(0.,20.2,0.));
#61966=CARTESIAN_POINT('',(-1.2490009027033E-15,-20.2,-2.47378653427765E-15));
#61967=CARTESIAN_POINT('Origin',(0.,0.,0.));
#61968=CARTESIAN_POINT('Origin',(0.1,0.,0.));
#61969=CARTESIAN_POINT('',(0.199999999999999,-20.5,-2.51052593825207E-15));
#61970=CARTESIAN_POINT('Origin',(0.2,0.,0.));
#61971=CARTESIAN_POINT('',(0.1,-20.35,-2.49215623626486E-15));
#61972=CARTESIAN_POINT('Origin',(1.2,0.,0.));
#61973=CARTESIAN_POINT('',(2.2,-20.5,-2.51052593825207E-15));
#61974=CARTESIAN_POINT('Origin',(2.2,0.,0.));
#61975=CARTESIAN_POINT('',(1.2,-20.5,-2.51052593825207E-15));
#61976=CARTESIAN_POINT('Origin',(2.3,0.,0.));
#61977=CARTESIAN_POINT('',(2.3,-20.35,-2.49215623626486E-15));
#71607=UNCERTAINTY_MEASURE_WITH_UNIT(LENGTH_MEASURE(0.01),#71629,
'DISTANCE_ACCURACY_VALUE',
'Maximum model space distance between geometric entities at asserted c
onnectivities');
#71613=UNCERTAINTY_MEASURE_WITH_UNIT(LENGTH_MEASURE(0.01),#71629,
'DISTANCE_ACCURACY_VALUE',
'Maximum model space distance between geometric entities at asserted c
onnectivities');
#71622=(
GEOMETRIC_REPRESENTATION_CONTEXT(3)
GLOBAL_UNCERTAINTY_ASSIGNED_CONTEXT((#71607))
GLOBAL_UNIT_ASSIGNED_CONTEXT((#71629,#71631,#71632))
REPRESENTATION_CONTEXT('','3D')
);
#71628=(
GEOMETRIC_REPRESENTATION_CONTEXT(3)
GLOBAL_UNCERTAINTY_ASSIGNED_CONTEXT((#71613))
GLOBAL_UNIT_ASSIGNED_CONTEXT((#71629,#71631,#71632))
REPRESENTATION_CONTEXT('','3D')
);
#71629=(
LENGTH_UNIT()
NAMED_UNIT(*)
SI_UNIT(.MILLI.,.METRE.)
);
#71631=(
NAMED_UNIT(*)
PLANE_ANGLE_UNIT()
SI_UNIT($,.RADIAN.)
);
#71632=(
NAMED_UNIT(*)
SI_UNIT($,.STERADIAN.)
SOLID_ANGLE_UNIT()
);
#71641=SHAPE_DEFINITION_REPRESENTATION(#71655,#71690);
#71655=PRODUCT_DEFINITION_SHAPE('',$,#71705);
#71690=SHAPE_REPRESENTATION('',(#37019),#71622);
#71696=PRODUCT_DEFINITION_CONTEXT('part definition',#71740,'design');
#71705=PRODUCT_DEFINITION('2026-10-25-00-23-54-288',
'11_Spindle_Tang_Washer_1in',#71719,#71696);
#71719=PRODUCT_DEFINITION_FORMATION('',$,#71750);
#71740=APPLICATION_CONTEXT(
'Core Data for Automotive Mechanical Design Process');
#71741=PRODUCT_CONTEXT('part definition',#71740,'mechanical');
#71750=PRODUCT('2026-10-25-00-23-54-288','11_Spindle_Tang_Washer_1in',$,
(#71741));
#71819=COLOUR_RGB('Black',0.12,0.14,0.17);
#71820=FILL_AREA_STYLE_COLOUR('',#71819);
#71821=FILL_AREA_STYLE('',(#71820));
#71822=SURFACE_STYLE_FILL_AREA(#71821);
#71823=SURFACE_SIDE_STYLE('',(#71822));
#71824=SURFACE_STYLE_USAGE(.BOTH.,#71823);
#71825=PRESENTATION_STYLE_ASSIGNMENT((#71824));
ENDSEC;
END-ISO-10303-21;
